ISO-10303-21;
HEADER;
FILE_DESCRIPTION (('STEP AP214'),
    '1' );
FILE_NAME ('Connecting Link.step',
    '2026-10-24T18:16:00',
    ( '' ),
    ( '' ),
    'SwSTEP 2.0',
    'SolidWorks 2025',
    '' );
FILE_SCHEMA (( 'AUTOMOTIVE_DESIGN' ));
ENDSEC;

DATA;
#20=DIRECTION ( 'NONE',  ( -0.000000000000000000, -0.000000000000000000, -1.000000000000000000 ) ) ;
#31=CARTESIAN_POINT ( 'NONE',  ( -1.181102362204724310, 0.000000000000000000, 0.02952755905511811330 ) ) ;
#50=DIRECTION ( 'NONE',  ( -0.000000000000000000, -0.000000000000000000, -1.000000000000000000 ) ) ;
#52=DIRECTION ( 'NONE',  ( 1.000000000000000000, 0.000000000000000000, -0.000000000000000000 ) ) ;
#66=DIRECTION ( 'NONE',  ( 1.000000000000000000, 0.000000000000000000, 0.000000000000000000 ) ) ;
#69=LENGTH_MEASURE_WITH_UNIT ( LENGTH_MEASURE( 0.02539999999999999897 ), #11905 );
#88=CARTESIAN_POINT ( 'NONE',  ( 1.181102362204724310, 4.044111181948214319E-16, -0.02559055118110236185 ) ) ;
#203=ORIENTED_EDGE ( 'NONE', *, *, #9789, .F. ) ;
#227=CARTESIAN_POINT ( 'NONE',  ( -1.181102362204724310, 0.000000000000000000, 0.02952755905511811330 ) ) ;
#287=EDGE_LOOP ( 'NONE', ( #11579, #13812, #203, #3433 ) ) ;
#294=FACE_OUTER_BOUND ( 'NONE', #5000, .T. ) ;
#319=CARTESIAN_POINT ( 'NONE',  ( 1.181102362204724310, 4.044111181948214319E-16, 0.02559055118110236185 ) ) ;
#352=EDGE_CURVE ( 'NONE', #10241, #8022, #13137, .T. ) ;
#357=EDGE_LOOP ( 'NONE', ( #2575, #14703, #6111, #12477 ) ) ;
#368=DIRECTION ( 'NONE',  ( 1.000000000000000000, 0.000000000000000000, 0.000000000000000000 ) ) ;
#384=ORIENTED_EDGE ( 'NONE', *, *, #12887, .F. ) ;
#456=DIRECTION ( 'NONE',  ( 1.000000000000000000, 0.000000000000000000, 0.000000000000000000 ) ) ;
#493=DIRECTION ( 'NONE',  ( 0.000000000000000000, 0.000000000000000000, -1.000000000000000000 ) ) ;
#516=ORIENTED_EDGE ( 'NONE', *, *, #6244, .T. ) ;
#521=( NAMED_UNIT ( * ) PLANE_ANGLE_UNIT ( ) SI_UNIT ( $, .RADIAN. ) );
#522=EDGE_CURVE ( 'NONE', #14099, #6733, #9902, .T. ) ;
#526=ADVANCED_FACE ( 'NONE', ( #4500 ), #6362, .T. ) ;
#539=CARTESIAN_POINT ( 'NONE',  ( -1.224409448818897461, 5.303588500244450842E-18, -0.02952755905511811330 ) ) ;
#543=EDGE_LOOP ( 'NONE', ( #6687, #8996, #6929, #6640, #1120 ) ) ;
#600=AXIS2_PLACEMENT_3D ( 'NONE', #3840, #12245, #2907 ) ;
#620=DIRECTION ( 'NONE',  ( 0.000000000000000000, 0.000000000000000000, -1.000000000000000000 ) ) ;
#624=VERTEX_POINT ( 'NONE', #8197 ) ;
#638=VECTOR ( 'NONE', #1019, 39.37007874015748143 ) ;
#706=DIRECTION ( 'NONE',  ( 1.000000000000000000, 0.000000000000000000, 0.000000000000000000 ) ) ;
#717=ORIENTED_EDGE ( 'NONE', *, *, #9997, .F. ) ;
#741=DIRECTION ( 'NONE',  ( 1.000000000000000000, 0.000000000000000000, 0.000000000000000000 ) ) ;
#798=ORIENTED_EDGE ( 'NONE', *, *, #7205, .T. ) ;
#803=CYLINDRICAL_SURFACE ( 'NONE', #15382, 0.1279527559055117780 ) ;
#834=DIRECTION ( 'NONE',  ( 0.000000000000000000, -1.000000000000000000, 0.000000000000000000 ) ) ;
#866=AXIS2_PLACEMENT_3D ( 'NONE', #3653, #8735, #8428 ) ;
#869=CARTESIAN_POINT ( 'NONE',  ( -1.181102362204724310, 0.000000000000000000, -0.02952755905511811330 ) ) ;
#876=CARTESIAN_POINT ( 'NONE',  ( -1.181102362204724310, 0.000000000000000000, -0.02952755905511811330 ) ) ;
#900=APPLICATION_CONTEXT ( 'automotive_design' ) ;
#901=EDGE_CURVE ( 'NONE', #8071, #4513, #9408, .T. ) ;
#906=VECTOR ( 'NONE', #11172, 39.37007874015748143 ) ;
#918=EDGE_CURVE ( 'NONE', #12092, #8071, #5647, .T. ) ;
#933=DIRECTION ( 'NONE',  ( 1.224646799147353207E-16, 1.000000000000000000, -0.000000000000000000 ) ) ;
#945=AXIS2_PLACEMENT_3D ( 'NONE', #4820, #8441, #8672 ) ;
#947=MECHANICAL_DESIGN_GEOMETRIC_PRESENTATION_REPRESENTATION('',(#3202),#15213);
#971=DIRECTION ( 'NONE',  ( 0.000000000000000000, 0.000000000000000000, 1.000000000000000000 ) ) ;
#972=AXIS2_PLACEMENT_3D ( 'NONE', #13362, #5995, #1533 ) ;
#983=ORIENTED_EDGE ( 'NONE', *, *, #1673, .T. ) ;
#1015=DIRECTION ( 'NONE',  ( 1.000000000000000000, 0.000000000000000000, 0.000000000000000000 ) ) ;
#1019=DIRECTION ( 'NONE',  ( -0.000000000000000000, -0.000000000000000000, -1.000000000000000000 ) ) ;
#1044=CARTESIAN_POINT ( 'NONE',  ( 1.181102362204724310, 4.044111181948214319E-16, 0.02559055118110236185 ) ) ;
#1066=CARTESIAN_POINT ( 'NONE',  ( 1.181102362204724310, 4.044111181948214319E-16, -0.02952755905511811330 ) ) ;
#1095=AXIS2_PLACEMENT_3D ( 'NONE', #3557, #11728, #2237 ) ;
#1120=ORIENTED_EDGE ( 'NONE', *, *, #4380, .T. ) ;
#1123=CIRCLE ( 'NONE', #15120, 0.003937007874015749712 ) ;
#1132=DIRECTION ( 'NONE',  ( 0.000000000000000000, -1.000000000000000000, 0.000000000000000000 ) ) ;
#1147=CARTESIAN_POINT ( 'NONE',  ( 1.181102362204724310, 4.044111181948214319E-16, -0.02559055118110236185 ) ) ;
#1158=TOROIDAL_SURFACE ( 'NONE', #8388, 0.04330708661417329020, 0.003937007874015747977 ) ;
#1161=ORIENTED_EDGE ( 'NONE', *, *, #8660, .F. ) ;
#1162=CIRCLE ( 'NONE', #14161, 0.003937007874015749712 ) ;
#1181=ORIENTED_EDGE ( 'NONE', *, *, #12010, .F. ) ;
#1206=TOROIDAL_SURFACE ( 'NONE', #3702, 0.04330708661417329020, 0.003937007874015747977 ) ;
#1212=ORIENTED_EDGE ( 'NONE', *, *, #12986, .T. ) ;
#1272=ADVANCED_FACE ( 'NONE', ( #12912 ), #7893, .F. ) ;
#1275=CARTESIAN_POINT ( 'NONE',  ( -1.181102362204724310, 0.000000000000000000, 0.02952755905511811330 ) ) ;
#1276=CARTESIAN_POINT ( 'NONE',  ( 1.224409448818897461, 4.044111181948214319E-16, -0.02952755905511811330 ) ) ;
#1298=PLANE ( 'NONE',  #5602 ) ;
#1314=( NAMED_UNIT ( * ) SI_UNIT ( $, .STERADIAN. ) SOLID_ANGLE_UNIT ( ) );
#1358=AXIS2_PLACEMENT_3D ( 'NONE', #1044, #9743, #14511 ) ;
#1385=AXIS2_PLACEMENT_3D ( 'NONE', #11855, #1132, #8316 ) ;
#1413=CYLINDRICAL_SURFACE ( 'NONE', #14624, 0.03937007874015751446 ) ;
#1420=CARTESIAN_POINT ( 'NONE',  ( 1.181102362204724310, -0.1279527559055113062, -0.02559055118110236185 ) ) ;
#1479=CARTESIAN_POINT ( 'NONE',  ( -1.181102362204724310, 0.000000000000000000, -0.02559055118110236185 ) ) ;
#1490=DIRECTION ( 'NONE',  ( 1.000000000000000000, 0.000000000000000000, 0.000000000000000000 ) ) ;
#1516=CARTESIAN_POINT ( 'NONE',  ( 1.181102362204724310, 4.044111181948214319E-16, 0.02952755905511811330 ) ) ;
#1525=DIRECTION ( 'NONE',  ( 0.000000000000000000, 0.000000000000000000, -1.000000000000000000 ) ) ;
#1528=ORIENTED_EDGE ( 'NONE', *, *, #4288, .F. ) ;
#1533=DIRECTION ( 'NONE',  ( 1.000000000000000000, 0.000000000000000000, 0.000000000000000000 ) ) ;
#1573=DIRECTION ( 'NONE',  ( 0.000000000000000000, 0.000000000000000000, 1.000000000000000000 ) ) ;
#1583=ORIENTED_EDGE ( 'NONE', *, *, #6988, .T. ) ;
#1603=ORIENTED_EDGE ( 'NONE', *, *, #8939, .F. ) ;
#1620=CARTESIAN_POINT ( 'NONE',  ( 1.181102362204724310, 4.044111181948214319E-16, 0.02559055118110236185 ) ) ;
#1635=VECTOR ( 'NONE', #6238, 39.37007874015748143 ) ;
#1646=EDGE_LOOP ( 'NONE', ( #5437, #10259, #3434, #3376 ) ) ;
#1659=EDGE_CURVE ( 'NONE', #11443, #4974, #9690, .T. ) ;
#1673=EDGE_CURVE ( 'NONE', #2506, #9877, #6922, .T. ) ;
#1680=EDGE_CURVE ( 'NONE', #8643, #5718, #2923, .T. ) ;
#1688=CIRCLE ( 'NONE', #5920, 0.03937007874015751446 ) ;
#1755=ADVANCED_FACE ( 'NONE', ( #12494 ), #9459, .T. ) ;
#1769=CARTESIAN_POINT ( 'NONE',  ( -1.309055118110236116, 0.000000000000000000, -0.02559055118110236185 ) ) ;
#1772=DIRECTION ( 'NONE',  ( 0.000000000000000000, 0.000000000000000000, -1.000000000000000000 ) ) ;
#1791=DIRECTION ( 'NONE',  ( 1.000000000000000000, 0.000000000000000000, 0.000000000000000000 ) ) ;
#1870=CARTESIAN_POINT ( 'NONE',  ( -1.181102362204724310, 0.1279527559055117225, 0.02952755905511811330 ) ) ;
#1871=DIRECTION ( 'NONE',  ( 0.000000000000000000, 0.000000000000000000, 1.000000000000000000 ) ) ;
#1879=VERTEX_POINT ( 'NONE', #1276 ) ;
#1892=TOROIDAL_SURFACE ( 'NONE', #9402, 0.04330708661417329020, 0.003937007874015747977 ) ;
#1948=DIRECTION ( 'NONE',  ( 0.000000000000000000, 0.000000000000000000, 1.000000000000000000 ) ) ;
#1978=ORIENTED_EDGE ( 'NONE', *, *, #7205, .F. ) ;
#1988=CARTESIAN_POINT ( 'NONE',  ( -1.181102362204724310, -0.1279527559055117225, -0.02559055118110236185 ) ) ;
#2033=EDGE_LOOP ( 'NONE', ( #4734, #13202, #8370, #9239, #1161 ) ) ;
#2058=CARTESIAN_POINT ( 'NONE',  ( -1.181102362204724310, -0.1240157480314959815, 0.02952755905511811330 ) ) ;
#2070=CARTESIAN_POINT ( 'NONE',  ( -1.137795275590550936, 0.000000000000000000, -0.02559055118110236185 ) ) ;
#2077=AXIS2_PLACEMENT_3D ( 'NONE', #4522, #9304, #2184 ) ;
#2100=CARTESIAN_POINT ( 'NONE',  ( 1.309055118110236116, 4.044111181948214319E-16, 0.02559055118110236185 ) ) ;
#2114=DIRECTION ( 'NONE',  ( -0.000000000000000000, -0.000000000000000000, -1.000000000000000000 ) ) ;
#2127=ORIENTED_EDGE ( 'NONE', *, *, #3979, .F. ) ;
#2169=LINE ( 'NONE', #1870, #11843 ) ;
#2171=AXIS2_PLACEMENT_3D ( 'NONE', #10144, #9993, #14933 ) ;
#2184=DIRECTION ( 'NONE',  ( 1.000000000000000000, 0.000000000000000000, 0.000000000000000000 ) ) ;
#2185=AXIS2_PLACEMENT_3D ( 'NONE', #7574, #12372, #3048 ) ;
#2223=EDGE_LOOP ( 'NONE', ( #6547, #14816, #3034, #4086 ) ) ;
#2237=DIRECTION ( 'NONE',  ( -1.000000000000000000, 0.000000000000000000, 0.000000000000000000 ) ) ;
#2242=DIRECTION ( 'NONE',  ( 1.000000000000000000, 0.000000000000000000, 0.000000000000000000 ) ) ;
#2257=( CONVERSION_BASED_UNIT ( 'INCH', #69 ) LENGTH_UNIT ( ) NAMED_UNIT ( #4338 ) );
#2263=VERTEX_POINT ( 'NONE', #11268 ) ;
#2264=EDGE_CURVE ( 'NONE', #12221, #8322, #2579, .T. ) ;
#2265=VERTEX_POINT ( 'NONE', #12898 ) ;
#2279=ORIENTED_EDGE ( 'NONE', *, *, #12012, .T. ) ;
#2282=ORIENTED_EDGE ( 'NONE', *, *, #8759, .T. ) ;
#2311=EDGE_CURVE ( 'NONE', #4513, #13444, #2169, .T. ) ;
#2342=ORIENTED_EDGE ( 'NONE', *, *, #1659, .F. ) ;
#2408=EDGE_CURVE ( 'NONE', #2265, #624, #7824, .T. ) ;
#2447=CIRCLE ( 'NONE', #11201, 0.003937007874015749712 ) ;
#2453=CARTESIAN_POINT ( 'NONE',  ( 1.181102362204724310, 4.044111181948214319E-16, -0.02952755905511811330 ) ) ;
#2482=DIRECTION ( 'NONE',  ( -1.000000000000000000, -0.000000000000000000, -0.000000000000000000 ) ) ;
#2506=VERTEX_POINT ( 'NONE', #13570 ) ;
#2507=ADVANCED_FACE ( 'NONE', ( #5258 ), #6444, .T. ) ;
#2536=FACE_OUTER_BOUND ( 'NONE', #9451, .T. ) ;
#2547=FACE_OUTER_BOUND ( 'NONE', #2787, .T. ) ;
#2557=EDGE_LOOP ( 'NONE', ( #3590, #7197 ) ) ;
#2575=ORIENTED_EDGE ( 'NONE', *, *, #12774, .F. ) ;
#2579=CIRCLE ( 'NONE', #3336, 0.04330708661417324162 ) ;
#2611=DIRECTION ( 'NONE',  ( 1.000000000000000000, -0.000000000000000000, -0.000000000000000000 ) ) ;
#2637=CIRCLE ( 'NONE', #8644, 0.003937007874015749712 ) ;
#2639=FACE_OUTER_BOUND ( 'NONE', #4352, .T. ) ;
#2640=LINE ( 'NONE', #7550, #14833 ) ;
#2656=AXIS2_PLACEMENT_3D ( 'NONE', #4257, #12500, #9046 ) ;
#2658=DIRECTION ( 'NONE',  ( -0.000000000000000000, -0.000000000000000000, -1.000000000000000000 ) ) ;
#2690=AXIS2_PLACEMENT_3D ( 'NONE', #10716, #933, #5831 ) ;
#2704=FACE_OUTER_BOUND ( 'NONE', #7858, .T. ) ;
#2707=AXIS2_PLACEMENT_3D ( 'NONE', #9499, #13959, #14105 ) ;
#2717=CIRCLE ( 'NONE', #972, 0.1279527559055117780 ) ;
#2718=PLANE ( 'NONE',  #945 ) ;
#2749=DIRECTION ( 'NONE',  ( 1.000000000000000000, 0.000000000000000000, 0.000000000000000000 ) ) ;
#2754=DIRECTION ( 'NONE',  ( -0.000000000000000000, -0.000000000000000000, -1.000000000000000000 ) ) ;
#2764=CARTESIAN_POINT ( 'NONE',  ( 1.181102362204724310, 4.044111181948214319E-16, -0.02952755905511811330 ) ) ;
#2770=ORIENTED_EDGE ( 'NONE', *, *, #14019, .T. ) ;
#2772=EDGE_LOOP ( 'NONE', ( #14701, #14993 ) ) ;
#2787=EDGE_LOOP ( 'NONE', ( #9470, #11496, #5471, #4708 ) ) ;
#2841=CARTESIAN_POINT ( 'NONE',  ( -1.181102362204724310, -0.1279527559055117225, 0.02952755905511811330 ) ) ;
#2871=ORIENTED_EDGE ( 'NONE', *, *, #11557, .F. ) ;
#2907=DIRECTION ( 'NONE',  ( 1.000000000000000000, 0.000000000000000000, 0.000000000000000000 ) ) ;
#2923=CIRCLE ( 'NONE', #8187, 0.003937007874015749712 ) ;
#2944=ADVANCED_FACE ( 'NONE', ( #7215 ), #13860, .T. ) ;
#2965=ORIENTED_EDGE ( 'NONE', *, *, #1680, .T. ) ;
#2994=CARTESIAN_POINT ( 'NONE',  ( -1.224409448818897461, 5.303588500244450842E-18, 0.02559055118110236185 ) ) ;
#3005=SHAPE_DEFINITION_REPRESENTATION ( #13914, #11075 ) ;
#3034=ORIENTED_EDGE ( 'NONE', *, *, #6840, .F. ) ;
#3048=DIRECTION ( 'NONE',  ( -1.000000000000000000, 1.224646799147361096E-16, 0.000000000000000000 ) ) ;
#3053=CARTESIAN_POINT ( 'NONE',  ( -1.181102362204724310, 0.1279527559055117225, 0.02559055118110236185 ) ) ;
#3088=CIRCLE ( 'NONE', #5821, 0.1279527559055117780 ) ;
#3117=CARTESIAN_POINT ( 'NONE',  ( -1.181102362204724310, 0.1279527559055117225, 0.02952755905511811330 ) ) ;
#3133=EDGE_LOOP ( 'NONE', ( #9123, #10954, #516, #9048 ) ) ;
#3141=AXIS2_PLACEMENT_3D ( 'NONE', #14247, #3347, #10485 ) ;
#3144=DIRECTION ( 'NONE',  ( 1.000000000000000000, 0.000000000000000000, 0.000000000000000000 ) ) ;
#3148=EDGE_LOOP ( 'NONE', ( #14254, #14639, #983, #6575, #5807, #13066 ) ) ;
#3149=CARTESIAN_POINT ( 'NONE',  ( 1.181102362204724310, 4.044111181948214319E-16, -0.02952755905511811330 ) ) ;
#3201=DIRECTION ( 'NONE',  ( 0.000000000000000000, -0.000000000000000000, -1.000000000000000000 ) ) ;
#3202=STYLED_ITEM('',(#15519),#14611);
#3266=DIRECTION ( 'NONE',  ( -0.000000000000000000, -0.000000000000000000, -1.000000000000000000 ) ) ;
#3275=ORIENTED_EDGE ( 'NONE', *, *, #9898, .F. ) ;
#3282=ORIENTED_EDGE ( 'NONE', *, *, #12364, .F. ) ;
#3324=AXIS2_PLACEMENT_3D ( 'NONE', #4436, #5591, #4856 ) ;
#3336=AXIS2_PLACEMENT_3D ( 'NONE', #11736, #15322, #1791 ) ;
#3346=FACE_OUTER_BOUND ( 'NONE', #4239, .T. ) ;
#3347=DIRECTION ( 'NONE',  ( 0.000000000000000000, -1.000000000000000000, 0.000000000000000000 ) ) ;
#3354=EDGE_LOOP ( 'NONE', ( #4633, #5849, #3718, #12963 ) ) ;
#3376=ORIENTED_EDGE ( 'NONE', *, *, #14019, .F. ) ;
#3398=FACE_BOUND ( 'NONE', #11761, .T. ) ;
#3409=AXIS2_PLACEMENT_3D ( 'NONE', #12897, #12978, #2242 ) ;
#3433=ORIENTED_EDGE ( 'NONE', *, *, #10545, .F. ) ;
#3434=ORIENTED_EDGE ( 'NONE', *, *, #13330, .F. ) ;
#3435=ORIENTED_EDGE ( 'NONE', *, *, #7014, .F. ) ;
#3456=CARTESIAN_POINT ( 'NONE',  ( -1.220472440944881720, 0.000000000000000000, 0.02952755905511811330 ) ) ;
#3462=CIRCLE ( 'NONE', #2707, 0.003937007874015749712 ) ;
#3467=ORIENTED_EDGE ( 'NONE', *, *, #11307, .F. ) ;
#3480=ORIENTED_EDGE ( 'NONE', *, *, #10260, .T. ) ;
#3512=CYLINDRICAL_SURFACE ( 'NONE', #12449, 0.03937007874015751446 ) ;
#3544=CYLINDRICAL_SURFACE ( 'NONE', #3874, 0.03937007874015751446 ) ;
#3557=CARTESIAN_POINT ( 'NONE',  ( -1.181102362204724310, 0.000000000000000000, 0.02952755905511811330 ) ) ;
#3590=ORIENTED_EDGE ( 'NONE', *, *, #12364, .T. ) ;
#3629=DIRECTION ( 'NONE',  ( 0.000000000000000000, 0.000000000000000000, 1.000000000000000000 ) ) ;
#3649=CIRCLE ( 'NONE', #3886, 0.03937007874015751446 ) ;
#3652=CARTESIAN_POINT ( 'NONE',  ( 1.181102362204724310, 4.044111181948214319E-16, 0.02559055118110236185 ) ) ;
#3653=CARTESIAN_POINT ( 'NONE',  ( -1.181102362204724310, 0.000000000000000000, -0.02559055118110236185 ) ) ;
#3658=EDGE_LOOP ( 'NONE', ( #2127, #3282, #1212, #3467 ) ) ;
#3675=AXIS2_PLACEMENT_3D ( 'NONE', #6422, #4235, #5168 ) ;
#3676=ADVANCED_FACE ( 'NONE', ( #15173 ), #10076, .T. ) ;
#3702=AXIS2_PLACEMENT_3D ( 'NONE', #9843, #3892, #368 ) ;
#3718=ORIENTED_EDGE ( 'NONE', *, *, #7387, .T. ) ;
#3732=FACE_BOUND ( 'NONE', #2772, .T. ) ;
#3741=CARTESIAN_POINT ( 'NONE',  ( -1.181102362204724310, -0.1240157480314959815, -0.02952755905511811330 ) ) ;
#3777=DIRECTION ( 'NONE',  ( -0.000000000000000000, -0.000000000000000000, -1.000000000000000000 ) ) ;
#3797=FACE_OUTER_BOUND ( 'NONE', #10459, .T. ) ;
#3809=DIRECTION ( 'NONE',  ( 0.000000000000000000, 0.000000000000000000, 1.000000000000000000 ) ) ;
#3821=DIRECTION ( 'NONE',  ( 0.000000000000000000, 0.000000000000000000, 1.000000000000000000 ) ) ;
#3826=EDGE_LOOP ( 'NONE', ( #8033, #2282, #798, #4253 ) ) ;
#3840=CARTESIAN_POINT ( 'NONE',  ( 1.181102362204724310, 4.044111181948214319E-16, 0.02952755905511811330 ) ) ;
#3858=TOROIDAL_SURFACE ( 'NONE', #866, 0.1240157480314959815, 0.003937007874015747977 ) ;
#3874=AXIS2_PLACEMENT_3D ( 'NONE', #31, #3777, #9573 ) ;
#3885=AXIS2_PLACEMENT_3D ( 'NONE', #2453, #7229, #14815 ) ;
#3886=AXIS2_PLACEMENT_3D ( 'NONE', #6337, #2754, #14756 ) ;
#3892=DIRECTION ( 'NONE',  ( 0.000000000000000000, 0.000000000000000000, 1.000000000000000000 ) ) ;
#3904=ORIENTED_EDGE ( 'NONE', *, *, #10075, .F. ) ;
#3926=AXIS2_PLACEMENT_3D ( 'NONE', #7830, #7758, #12548 ) ;
#3946=CYLINDRICAL_SURFACE ( 'NONE', #9423, 0.03937007874015751446 ) ;
#3951=CARTESIAN_POINT ( 'NONE',  ( 1.181102362204724310, 0.1240157480314963978, 0.02559055118110236185 ) ) ;
#3958=DIRECTION ( 'NONE',  ( 0.000000000000000000, 0.000000000000000000, 1.000000000000000000 ) ) ;
#3979=EDGE_CURVE ( 'NONE', #9040, #12795, #5073, .T. ) ;
#4042=ORIENTED_EDGE ( 'NONE', *, *, #901, .F. ) ;
#4086=ORIENTED_EDGE ( 'NONE', *, *, #9481, .T. ) ;
#4169=EDGE_LOOP ( 'NONE', ( #7404, #5579, #5175, #6829 ) ) ;
#4177=PRODUCT_CONTEXT ( 'NONE', #900, 'mechanical' ) ;
#4187=CIRCLE ( 'NONE', #2690, 0.003937007874015724558 ) ;
#4212=DIRECTION ( 'NONE',  ( 1.000000000000000000, 0.000000000000000000, 0.000000000000000000 ) ) ;
#4235=DIRECTION ( 'NONE',  ( 0.000000000000000000, 0.000000000000000000, 1.000000000000000000 ) ) ;
#4239=EDGE_LOOP ( 'NONE', ( #12833, #1528, #12404, #10080 ) ) ;
#4253=ORIENTED_EDGE ( 'NONE', *, *, #7387, .F. ) ;
#4257=CARTESIAN_POINT ( 'NONE',  ( 1.181102362204724310, 4.044111181948214319E-16, 0.02952755905511811330 ) ) ;
#4264=DIRECTION ( 'NONE',  ( 0.000000000000000000, 0.000000000000000000, 1.000000000000000000 ) ) ;
#4288=EDGE_CURVE ( 'NONE', #15235, #10603, #13566, .T. ) ;
#4315=DIRECTION ( 'NONE',  ( 0.000000000000000000, 0.000000000000000000, 1.000000000000000000 ) ) ;
#4338=DIMENSIONAL_EXPONENTS ( 1.000000000000000000, 0.000000000000000000, 0.000000000000000000, 0.000000000000000000, 0.000000000000000000, 0.000000000000000000, 0.000000000000000000 ) ;
#4352=EDGE_LOOP ( 'NONE', ( #7071, #8143, #4042, #14194 ) ) ;
#4360=CARTESIAN_POINT ( 'NONE',  ( 1.181102362204724310, 4.044111181948214319E-16, 0.02952755905511811330 ) ) ;
#4364=CARTESIAN_POINT ( 'NONE',  ( -1.181102362204724310, -0.1240157480314959815, -0.02952755905511811330 ) ) ;
#4373=AXIS2_PLACEMENT_3D ( 'NONE', #1147, #14061, #13113 ) ;
#4380=EDGE_CURVE ( 'NONE', #5718, #12092, #14108, .T. ) ;
#4381=CIRCLE ( 'NONE', #3885, 0.1240157480314959260 ) ;
#4427=CARTESIAN_POINT ( 'NONE',  ( 1.141732283464566677, 4.044111181948214319E-16, 0.02952755905511811330 ) ) ;
#4436=CARTESIAN_POINT ( 'NONE',  ( -1.181102362204724310, 0.000000000000000000, -0.02559055118110236185 ) ) ;
#4458=CARTESIAN_POINT ( 'NONE',  ( -1.181102362204724310, 0.000000000000000000, 0.02952755905511811330 ) ) ;
#4485=FACE_BOUND ( 'NONE', #2557, .T. ) ;
#4500=FACE_OUTER_BOUND ( 'NONE', #2033, .T. ) ;
#4513=VERTEX_POINT ( 'NONE', #3053 ) ;
#4520=DIRECTION ( 'NONE',  ( -1.000000000000000000, 0.000000000000000000, 0.000000000000000000 ) ) ;
#4522=CARTESIAN_POINT ( 'NONE',  ( -1.181102362204724310, 0.000000000000000000, 0.02559055118110236185 ) ) ;
#4546=ORIENTED_EDGE ( 'NONE', *, *, #5612, .T. ) ;
#4625=DIRECTION ( 'NONE',  ( 0.000000000000000000, 0.000000000000000000, 1.000000000000000000 ) ) ;
#4633=ORIENTED_EDGE ( 'NONE', *, *, #8759, .F. ) ;
#4635=ORIENTED_EDGE ( 'NONE', *, *, #9481, .F. ) ;
#4636=AXIS2_PLACEMENT_3D ( 'NONE', #10987, #5017, #11048 ) ;
#4665=CIRCLE ( 'NONE', #2171, 0.1240157480314959260 ) ;
#4684=TOROIDAL_SURFACE ( 'NONE', #3675, 0.04330708661417329020, 0.003937007874015747977 ) ;
#4708=ORIENTED_EDGE ( 'NONE', *, *, #12986, .F. ) ;
#4714=ADVANCED_FACE ( 'NONE', ( #4772 ), #5342, .T. ) ;
#4727=FACE_OUTER_BOUND ( 'NONE', #12742, .T. ) ;
#4734=ORIENTED_EDGE ( 'NONE', *, *, #901, .T. ) ;
#4746=DIRECTION ( 'NONE',  ( -0.000000000000000000, -0.000000000000000000, -1.000000000000000000 ) ) ;
#4756=CARTESIAN_POINT ( 'NONE',  ( -1.181102362204724310, -0.1240157480314959815, -0.02559055118110236185 ) ) ;
#4762=VERTEX_POINT ( 'NONE', #539 ) ;
#4772=FACE_OUTER_BOUND ( 'NONE', #3133, .T. ) ;
#4773=ADVANCED_FACE ( 'NONE', ( #12146 ), #1413, .F. ) ;
#4806=LINE ( 'NONE', #13348, #14668 ) ;
#4811=CARTESIAN_POINT ( 'NONE',  ( -1.181102362204724310, -0.1240157480314959815, 0.02559055118110236185 ) ) ;
#4820=CARTESIAN_POINT ( 'NONE',  ( -1.181102362204724310, -0.1279527559055117225, 0.02952755905511811330 ) ) ;
#4856=DIRECTION ( 'NONE',  ( 1.000000000000000000, 0.000000000000000000, 0.000000000000000000 ) ) ;
#4871=VERTEX_POINT ( 'NONE', #4364 ) ;
#4900=ORIENTED_EDGE ( 'NONE', *, *, #11557, .T. ) ;
#4930=DIRECTION ( 'NONE',  ( 0.000000000000000000, 0.000000000000000000, 1.000000000000000000 ) ) ;
#4949=AXIS2_PLACEMENT_3D ( 'NONE', #319, #20, #9876 ) ;
#4971=CARTESIAN_POINT ( 'NONE',  ( 1.137795275590550936, 4.097147066950659020E-16, 0.02559055118110236185 ) ) ;
#4974=VERTEX_POINT ( 'NONE', #15187 ) ;
#4979=CARTESIAN_POINT ( 'NONE',  ( -1.181102362204724310, 0.1240157480314959815, 0.02559055118110236185 ) ) ;
#4980=CARTESIAN_POINT ( 'NONE',  ( 1.181102362204724310, 4.044111181948214319E-16, -0.02559055118110236185 ) ) ;
#5000=EDGE_LOOP ( 'NONE', ( #3904, #1978, #6203, #3275 ) ) ;
#5017=DIRECTION ( 'NONE',  ( 0.000000000000000000, 0.000000000000000000, 1.000000000000000000 ) ) ;
#5033=CARTESIAN_POINT ( 'NONE',  ( -1.181102362204724310, 0.1240157480314959815, 0.02952755905511811330 ) ) ;
#5041=DIRECTION ( 'NONE',  ( -0.000000000000000000, -0.000000000000000000, -1.000000000000000000 ) ) ;
#5042=CARTESIAN_POINT ( 'NONE',  ( 1.141732283464566677, 4.044111181948214319E-16, 0.02559055118110236185 ) ) ;
#5048=DIRECTION ( 'NONE',  ( 1.000000000000000000, 0.000000000000000000, 0.000000000000000000 ) ) ;
#5060=CARTESIAN_POINT ( 'NONE',  ( -1.181102362204724310, 0.000000000000000000, 0.02559055118110236185 ) ) ;
#5073=CIRCLE ( 'NONE', #7089, 0.003937007874015724558 ) ;
#5091=AXIS2_PLACEMENT_3D ( 'NONE', #1275, #9665, #7365 ) ;
#5106=PRODUCT_DEFINITION_FORMATION_WITH_SPECIFIED_SOURCE ( 'ANY', '', #8171, .NOT_KNOWN. ) ;
#5124=CIRCLE ( 'NONE', #4636, 0.1279527559055117780 ) ;
#5134=CARTESIAN_POINT ( 'NONE',  ( -1.309055118110236116, 0.000000000000000000, 0.02952755905511811330 ) ) ;
#5164=AXIS2_PLACEMENT_3D ( 'NONE', #3149, #7927, #10579 ) ;
#5168=DIRECTION ( 'NONE',  ( 1.000000000000000000, 0.000000000000000000, 0.000000000000000000 ) ) ;
#5170=DIRECTION ( 'NONE',  ( 1.000000000000000000, 0.000000000000000000, 0.000000000000000000 ) ) ;
#5173=ADVANCED_FACE ( 'NONE', ( #3346 ), #10923, .T. ) ;
#5175=ORIENTED_EDGE ( 'NONE', *, *, #7926, .F. ) ;
#5215=EDGE_CURVE ( 'NONE', #6019, #12169, #5424, .T. ) ;
#5218=ORIENTED_EDGE ( 'NONE', *, *, #8555, .F. ) ;
#5258=FACE_OUTER_BOUND ( 'NONE', #9608, .T. ) ;
#5270=SHAPE_REPRESENTATION_RELATIONSHIP ( 'NONE' , 'NONE' ,  #11075, #11164 ) ;
#5281=VERTEX_POINT ( 'NONE', #10052 ) ;
#5312=VECTOR ( 'NONE', #6476, 39.37007874015748143 ) ;
#5319=CARTESIAN_POINT ( 'NONE',  ( -1.137795275590550936, 0.000000000000000000, -0.02952755905511811330 ) ) ;
#5333=DIRECTION ( 'NONE',  ( -1.000000000000000000, 0.000000000000000000, 0.000000000000000000 ) ) ;
#5338=DIRECTION ( 'NONE',  ( -1.000000000000000000, 0.000000000000000000, 0.000000000000000000 ) ) ;
#5342=TOROIDAL_SURFACE ( 'NONE', #7353, 0.04330708661417329020, 0.003937007874015747977 ) ;
#5411=CIRCLE ( 'NONE', #3926, 0.003937007874015749712 ) ;
#5424=LINE ( 'NONE', #2841, #5856 ) ;
#5430=CARTESIAN_POINT ( 'NONE',  ( -1.181102362204724310, 0.1279527559055117225, -0.02559055118110236185 ) ) ;
#5437=ORIENTED_EDGE ( 'NONE', *, *, #2408, .F. ) ;
#5441=DIRECTION ( 'NONE',  ( 1.000000000000000000, 0.000000000000000000, 0.000000000000000000 ) ) ;
#5455=AXIS2_PLACEMENT_3D ( 'NONE', #227, #5041, #9842 ) ;
#5471=ORIENTED_EDGE ( 'NONE', *, *, #11123, .F. ) ;
#5488=ORIENTED_EDGE ( 'NONE', *, *, #15357, .T. ) ;
#5545=CARTESIAN_POINT ( 'NONE',  ( 1.141732283464566677, 4.044111181948214319E-16, -0.02559055118110236185 ) ) ;
#5573=ADVANCED_FACE ( 'NONE', ( #4727 ), #3544, .F. ) ;
#5579=ORIENTED_EDGE ( 'NONE', *, *, #5612, .F. ) ;
#5591=DIRECTION ( 'NONE',  ( 0.000000000000000000, 0.000000000000000000, 1.000000000000000000 ) ) ;
#5600=EDGE_CURVE ( 'NONE', #2265, #2506, #14898, .T. ) ;
#5602=AXIS2_PLACEMENT_3D ( 'NONE', #14378, #3958, #52 ) ;
#5612=EDGE_CURVE ( 'NONE', #10603, #2265, #4381, .T. ) ;
#5647=LINE ( 'NONE', #12789, #12403 ) ;
#5677=DIRECTION ( 'NONE',  ( -1.000000000000000000, 0.000000000000000000, 0.000000000000000000 ) ) ;
#5689=FACE_OUTER_BOUND ( 'NONE', #3826, .T. ) ;
#5718=VERTEX_POINT ( 'NONE', #11451 ) ;
#5807=ORIENTED_EDGE ( 'NONE', *, *, #7777, .T. ) ;
#5821=AXIS2_PLACEMENT_3D ( 'NONE', #14783, #11408, #7878 ) ;
#5831=DIRECTION ( 'NONE',  ( -1.000000000000000000, 1.224646799147296261E-16, 0.000000000000000000 ) ) ;
#5849=ORIENTED_EDGE ( 'NONE', *, *, #9997, .T. ) ;
#5852=DIRECTION ( 'NONE',  ( 0.000000000000000000, 0.000000000000000000, 1.000000000000000000 ) ) ;
#5856=VECTOR ( 'NONE', #7621, 39.37007874015748143 ) ;
#5880=DIRECTION ( 'NONE',  ( -1.000000000000000000, 0.000000000000000000, 0.000000000000000000 ) ) ;
#5920=AXIS2_PLACEMENT_3D ( 'NONE', #10251, #1871, #706 ) ;
#5945=LINE ( 'NONE', #3456, #12976 ) ;
#5995=DIRECTION ( 'NONE',  ( -0.000000000000000000, -0.000000000000000000, -1.000000000000000000 ) ) ;
#6019=VERTEX_POINT ( 'NONE', #13060 ) ;
#6029=EDGE_LOOP ( 'NONE', ( #5488, #11387, #4900, #6551 ) ) ;
#6047=ADVANCED_FACE ( 'NONE', ( #8446 ), #12412, .T. ) ;
#6057=AXIS2_PLACEMENT_3D ( 'NONE', #11013, #13370, #3809 ) ;
#6100=CARTESIAN_POINT ( 'NONE',  ( 1.220472440944881720, 4.092325622859527280E-16, -0.02559055118110236185 ) ) ;
#6111=ORIENTED_EDGE ( 'NONE', *, *, #10813, .T. ) ;
#6121=CIRCLE ( 'NONE', #13399, 0.1279527559055117780 ) ;
#6136=FACE_BOUND ( 'NONE', #7836, .T. ) ;
#6156=( NAMED_UNIT ( * ) PLANE_ANGLE_UNIT ( ) SI_UNIT ( $, .RADIAN. ) );
#6178=EDGE_CURVE ( 'NONE', #11619, #10362, #7490, .T. ) ;
#6203=ORIENTED_EDGE ( 'NONE', *, *, #12887, .T. ) ;
#6238=DIRECTION ( 'NONE',  ( -0.000000000000000000, -0.000000000000000000, -1.000000000000000000 ) ) ;
#6244=EDGE_CURVE ( 'NONE', #8322, #8022, #1162, .T. ) ;
#6314=ORIENTED_EDGE ( 'NONE', *, *, #10953, .F. ) ;
#6337=CARTESIAN_POINT ( 'NONE',  ( -1.181102362204724310, 0.000000000000000000, -0.02559055118110236185 ) ) ;
#6344=AXIS2_PLACEMENT_3D ( 'NONE', #3117, #834, #3201 ) ;
#6362=TOROIDAL_SURFACE ( 'NONE', #14900, 0.1240157480314959815, 0.003937007874015747977 ) ;
#6366=CIRCLE ( 'NONE', #3141, 0.003937007874015749712 ) ;
#6380=DIRECTION ( 'NONE',  ( 0.000000000000000000, 0.000000000000000000, 1.000000000000000000 ) ) ;
#6422=CARTESIAN_POINT ( 'NONE',  ( -1.181102362204724310, 0.000000000000000000, 0.02559055118110236185 ) ) ;
#6435=ADVANCED_FACE ( 'NONE', ( #7466 ), #3946, .F. ) ;
#6439=CARTESIAN_POINT ( 'NONE',  ( -1.181102362204724310, 0.000000000000000000, 0.02952755905511811330 ) ) ;
#6444=CYLINDRICAL_SURFACE ( 'NONE', #10104, 0.003937007874015749712 ) ;
#6460=LENGTH_MEASURE_WITH_UNIT ( LENGTH_MEASURE( 0.02539999999999999897 ), #9999 );
#6476=DIRECTION ( 'NONE',  ( -0.000000000000000000, -0.000000000000000000, -1.000000000000000000 ) ) ;
#6507=FACE_OUTER_BOUND ( 'NONE', #9574, .T. ) ;
#6541=DIRECTION ( 'NONE',  ( 1.000000000000000000, 0.000000000000000000, 0.000000000000000000 ) ) ;
#6543=CARTESIAN_POINT ( 'NONE',  ( 1.224409448818897461, 4.044111181948214319E-16, -0.02559055118110236185 ) ) ;
#6547=ORIENTED_EDGE ( 'NONE', *, *, #5215, .T. ) ;
#6551=ORIENTED_EDGE ( 'NONE', *, *, #5215, .F. ) ;
#6575=ORIENTED_EDGE ( 'NONE', *, *, #13446, .F. ) ;
#6577=CARTESIAN_POINT ( 'NONE',  ( -1.181102362204724310, 0.1240157480314959815, 0.02559055118110236185 ) ) ;
#6578=AXIS2_PLACEMENT_3D ( 'NONE', #4756, #2482, #7322 ) ;
#6580=VECTOR ( 'NONE', #7620, 39.37007874015748143 ) ;
#6591=LINE ( 'NONE', #5430, #13176 ) ;
#6602=DIRECTION ( 'NONE',  ( -0.000000000000000000, -0.000000000000000000, -1.000000000000000000 ) ) ;
#6640=ORIENTED_EDGE ( 'NONE', *, *, #9503, .T. ) ;
#6657=CIRCLE ( 'NONE', #12197, 0.04330708661417324162 ) ;
#6683=AXIS2_PLACEMENT_3D ( 'NONE', #11406, #13824, #11247 ) ;
#6687=ORIENTED_EDGE ( 'NONE', *, *, #918, .T. ) ;
#6705=ORIENTED_EDGE ( 'NONE', *, *, #10139, .T. ) ;
#6733=VERTEX_POINT ( 'NONE', #6100 ) ;
#6754=CARTESIAN_POINT ( 'NONE',  ( 1.224409448818897461, 4.044111181948214319E-16, 0.02952755905511811330 ) ) ;
#6786=ORIENTED_EDGE ( 'NONE', *, *, #9898, .T. ) ;
#6790=ORIENTED_EDGE ( 'NONE', *, *, #12774, .T. ) ;
#6818=CARTESIAN_POINT ( 'NONE',  ( 1.305118110236220152, 4.044111181948214319E-16, 0.02559055118110236185 ) ) ;
#6829=ORIENTED_EDGE ( 'NONE', *, *, #1673, .F. ) ;
#6840=EDGE_CURVE ( 'NONE', #11443, #14199, #9001, .T. ) ;
#6848=VECTOR ( 'NONE', #15164, 39.37007874015748143 ) ;
#6922=CIRCLE ( 'NONE', #14439, 0.1279527559055117780 ) ;
#6928=ORIENTED_EDGE ( 'NONE', *, *, #6178, .F. ) ;
#6929=ORIENTED_EDGE ( 'NONE', *, *, #10953, .T. ) ;
#6939=DIRECTION ( 'NONE',  ( -0.000000000000000000, -0.000000000000000000, -1.000000000000000000 ) ) ;
#6959=CARTESIAN_POINT ( 'NONE',  ( -1.181102362204724310, 0.000000000000000000, -0.02559055118110236185 ) ) ;
#6988=EDGE_CURVE ( 'NONE', #8322, #12221, #14853, .T. ) ;
#6993=CARTESIAN_POINT ( 'NONE',  ( 1.137795275590550936, 4.097147066950659020E-16, -0.02952755905511811330 ) ) ;
#7008=DIRECTION ( 'NONE',  ( 0.000000000000000000, 0.000000000000000000, 1.000000000000000000 ) ) ;
#7014=EDGE_CURVE ( 'NONE', #4871, #12169, #9602, .T. ) ;
#7071=ORIENTED_EDGE ( 'NONE', *, *, #12010, .T. ) ;
#7085=CYLINDRICAL_SURFACE ( 'NONE', #8420, 0.003937007874015749712 ) ;
#7089=AXIS2_PLACEMENT_3D ( 'NONE', #2994, #14989, #9026 ) ;
#7140=ORIENTED_EDGE ( 'NONE', *, *, #10813, .F. ) ;
#7143=AXIS2_PLACEMENT_3D ( 'NONE', #4979, #9777, #14481 ) ;
#7187=AXIS2_PLACEMENT_3D ( 'NONE', #11425, #1948, #6541 ) ;
#7195=LINE ( 'NONE', #11757, #638 ) ;
#7197=ORIENTED_EDGE ( 'NONE', *, *, #10361, .T. ) ;
#7205=EDGE_CURVE ( 'NONE', #6733, #14099, #10337, .T. ) ;
#7215=FACE_OUTER_BOUND ( 'NONE', #1646, .T. ) ;
#7229=DIRECTION ( 'NONE',  ( -0.000000000000000000, -0.000000000000000000, -1.000000000000000000 ) ) ;
#7261=DIRECTION ( 'NONE',  ( 0.000000000000000000, 0.000000000000000000, 1.000000000000000000 ) ) ;
#7276=ORIENTED_EDGE ( 'NONE', *, *, #522, .F. ) ;
#7322=DIRECTION ( 'NONE',  ( 0.000000000000000000, 0.000000000000000000, 1.000000000000000000 ) ) ;
#7334=ORIENTED_EDGE ( 'NONE', *, *, #1659, .T. ) ;
#7353=AXIS2_PLACEMENT_3D ( 'NONE', #15441, #4930, #8296 ) ;
#7365=DIRECTION ( 'NONE',  ( 1.000000000000000000, 0.000000000000000000, -0.000000000000000000 ) ) ;
#7378=AXIS2_PLACEMENT_3D ( 'NONE', #9722, #14493, #8522 ) ;
#7387=EDGE_CURVE ( 'NONE', #10241, #14099, #9134, .T. ) ;
#7404=ORIENTED_EDGE ( 'NONE', *, *, #5600, .F. ) ;
#7411=DIRECTION ( 'NONE',  ( -1.000000000000000000, -0.000000000000000000, 0.000000000000000000 ) ) ;
#7412=CYLINDRICAL_SURFACE ( 'NONE', #7143, 0.003937007874015749712 ) ;
#7413=DIRECTION ( 'NONE',  ( 1.000000000000000000, 0.000000000000000000, 0.000000000000000000 ) ) ;
#7466=FACE_OUTER_BOUND ( 'NONE', #3354, .T. ) ;
#7474=DIRECTION ( 'NONE',  ( 1.000000000000000000, 0.000000000000000000, 0.000000000000000000 ) ) ;
#7475=CARTESIAN_POINT ( 'NONE',  ( 1.220472440944881720, 4.092325622859527280E-16, 0.02559055118110236185 ) ) ;
#7489=DIRECTION ( 'NONE',  ( 1.000000000000000000, 0.000000000000000000, 0.000000000000000000 ) ) ;
#7490=LINE ( 'NONE', #5134, #906 ) ;
#7518=EDGE_CURVE ( 'NONE', #4513, #8855, #9526, .T. ) ;
#7534=DIRECTION ( 'NONE',  ( 0.000000000000000000, 0.000000000000000000, 1.000000000000000000 ) ) ;
#7550=CARTESIAN_POINT ( 'NONE',  ( -1.181102362204724310, -0.1279527559055117225, -0.02559055118110236185 ) ) ;
#7566=CARTESIAN_POINT ( 'NONE',  ( -1.181102362204724310, 0.000000000000000000, 0.02952755905511811330 ) ) ;
#7567=FACE_OUTER_BOUND ( 'NONE', #7698, .T. ) ;
#7573=ORIENTED_EDGE ( 'NONE', *, *, #2408, .T. ) ;
#7574=CARTESIAN_POINT ( 'NONE',  ( -1.224409448818897461, 5.303588500244450842E-18, -0.02559055118110236185 ) ) ;
#7590=CARTESIAN_POINT ( 'NONE',  ( 1.181102362204724310, 0.1240157480314959815, -0.02952755905511811330 ) ) ;
#7620=DIRECTION ( 'NONE',  ( 1.000000000000000000, -0.000000000000000000, -0.000000000000000000 ) ) ;
#7621=DIRECTION ( 'NONE',  ( -0.000000000000000000, -0.000000000000000000, -1.000000000000000000 ) ) ;
#7651=AXIS2_PLACEMENT_3D ( 'NONE', #6959, #11752, #1015 ) ;
#7666=CARTESIAN_POINT ( 'NONE',  ( -1.220472440944881720, 0.000000000000000000, 0.02559055118110236185 ) ) ;
#7698=EDGE_LOOP ( 'NONE', ( #12765, #12632, #717, #12243 ) ) ;
#7713=CYLINDRICAL_SURFACE ( 'NONE', #2656, 0.1279527559055117780 ) ;
#7732=ORIENTED_EDGE ( 'NONE', *, *, #8939, .T. ) ;
#7758=DIRECTION ( 'NONE',  ( -1.000000000000000000, -0.000000000000000000, -0.000000000000000000 ) ) ;
#7770=DIRECTION ( 'NONE',  ( -0.000000000000000000, -0.000000000000000000, -1.000000000000000000 ) ) ;
#7777=EDGE_CURVE ( 'NONE', #8855, #8643, #13123, .T. ) ;
#7824=CIRCLE ( 'NONE', #8576, 0.1240157480314959260 ) ;
#7830=CARTESIAN_POINT ( 'NONE',  ( 1.181102362204724310, -0.1240157480314955790, -0.02559055118110236185 ) ) ;
#7836=EDGE_LOOP ( 'NONE', ( #2279, #6786 ) ) ;
#7849=CARTESIAN_POINT ( 'NONE',  ( 1.181102362204724310, 0.1240157480314959815, 0.02952755905511811330 ) ) ;
#7858=EDGE_LOOP ( 'NONE', ( #14501, #12249, #11743, #2871, #5218 ) ) ;
#7878=DIRECTION ( 'NONE',  ( 1.000000000000000000, 0.000000000000000000, 0.000000000000000000 ) ) ;
#7893=PLANE ( 'NONE',  #6344 ) ;
#7906=CIRCLE ( 'NONE', #3409, 0.1279527559055117780 ) ;
#7926=EDGE_CURVE ( 'NONE', #9877, #10603, #1123, .T. ) ;
#7927=DIRECTION ( 'NONE',  ( 0.000000000000000000, 0.000000000000000000, 1.000000000000000000 ) ) ;
#7932=VECTOR ( 'NONE', #10883, 39.37007874015748143 ) ;
#7938=DIRECTION ( 'NONE',  ( 0.000000000000000000, -1.000000000000000000, 0.000000000000000000 ) ) ;
#7964=ORIENTED_EDGE ( 'NONE', *, *, #4380, .F. ) ;
#7987=ADVANCED_FACE ( 'NONE', ( #6136, #3732, #3797 ), #1298, .F. ) ;
#8003=ADVANCED_FACE ( 'NONE', ( #2704 ), #3858, .T. ) ;
#8022=VERTEX_POINT ( 'NONE', #7475 ) ;
#8033=ORIENTED_EDGE ( 'NONE', *, *, #352, .T. ) ;
#8037=DIRECTION ( 'NONE',  ( 1.000000000000000000, 0.000000000000000000, 0.000000000000000000 ) ) ;
#8071=VERTEX_POINT ( 'NONE', #5033 ) ;
#8105=CARTESIAN_POINT ( 'NONE',  ( -1.181102362204724310, 0.000000000000000000, 0.02559055118110236185 ) ) ;
#8143=ORIENTED_EDGE ( 'NONE', *, *, #7518, .F. ) ;
#8149=AXIS2_PLACEMENT_3D ( 'NONE', #6577, #5880, #971 ) ;
#8165=CIRCLE ( 'NONE', #15417, 0.03937007874015751446 ) ;
#8171=PRODUCT ( 'Connecting Link', 'Connecting Link', '', ( #4177 ) ) ;
#8187=AXIS2_PLACEMENT_3D ( 'NONE', #6818, #7938, #11296 ) ;
#8197=CARTESIAN_POINT ( 'NONE',  ( 1.181102362204724310, -0.1240157480314955790, -0.02952755905511811330 ) ) ;
#8255=EDGE_LOOP ( 'NONE', ( #7276, #10711, #15237, #384 ) ) ;
#8281=CARTESIAN_POINT ( 'NONE',  ( 1.181102362204724310, 4.044111181948214319E-16, 0.02952755905511811330 ) ) ;
#8296=DIRECTION ( 'NONE',  ( 1.000000000000000000, 0.000000000000000000, 0.000000000000000000 ) ) ;
#8316=DIRECTION ( 'NONE',  ( 0.000000000000000000, 0.000000000000000000, -1.000000000000000000 ) ) ;
#8322=VERTEX_POINT ( 'NONE', #6754 ) ;
#8329=TOROIDAL_SURFACE ( 'NONE', #11583, 0.1240157480314959815, 0.003937007874015747977 ) ;
#8370=ORIENTED_EDGE ( 'NONE', *, *, #15357, .F. ) ;
#8388=AXIS2_PLACEMENT_3D ( 'NONE', #12229, #3821, #9791 ) ;
#8420=AXIS2_PLACEMENT_3D ( 'NONE', #4811, #5677, #3629 ) ;
#8426=DIRECTION ( 'NONE',  ( 0.000000000000000000, 0.000000000000000000, 1.000000000000000000 ) ) ;
#8428=DIRECTION ( 'NONE',  ( 1.000000000000000000, 0.000000000000000000, 0.000000000000000000 ) ) ;
#8441=DIRECTION ( 'NONE',  ( 0.000000000000000000, 1.000000000000000000, 0.000000000000000000 ) ) ;
#8446=FACE_OUTER_BOUND ( 'NONE', #14992, .T. ) ;
#8452=ORIENTED_EDGE ( 'NONE', *, *, #4288, .T. ) ;
#8497=CARTESIAN_POINT ( 'NONE',  ( 1.181102362204724310, 0.1279527559055117225, 0.02559055118110236185 ) ) ;
#8517=CARTESIAN_POINT ( 'NONE',  ( -1.224409448818897461, 5.303588500244450842E-18, 0.02952755905511811330 ) ) ;
#8522=DIRECTION ( 'NONE',  ( 1.000000000000000000, 0.000000000000000000, 0.000000000000000000 ) ) ;
#8555=EDGE_CURVE ( 'NONE', #13444, #10362, #5124, .T. ) ;
#8562=EDGE_CURVE ( 'NONE', #5281, #11243, #3649, .T. ) ;
#8576=AXIS2_PLACEMENT_3D ( 'NONE', #1066, #4746, #14377 ) ;
#8606=FACE_OUTER_BOUND ( 'NONE', #8255, .T. ) ;
#8626=DIRECTION ( 'NONE',  ( -0.000000000000000000, -0.000000000000000000, -1.000000000000000000 ) ) ;
#8643=VERTEX_POINT ( 'NONE', #2100 ) ;
#8644=AXIS2_PLACEMENT_3D ( 'NONE', #6543, #14964, #620 ) ;
#8660=EDGE_CURVE ( 'NONE', #8071, #9541, #11136, .T. ) ;
#8666=AXIS2_PLACEMENT_3D ( 'NONE', #4971, #9769, #13352 ) ;
#8672=DIRECTION ( 'NONE',  ( 0.000000000000000000, -0.000000000000000000, 1.000000000000000000 ) ) ;
#8729=DIRECTION ( 'NONE',  ( 0.000000000000000000, 0.000000000000000000, 1.000000000000000000 ) ) ;
#8735=DIRECTION ( 'NONE',  ( 0.000000000000000000, 0.000000000000000000, 1.000000000000000000 ) ) ;
#8759=EDGE_CURVE ( 'NONE', #8022, #6733, #7195, .T. ) ;
#8784=FACE_OUTER_BOUND ( 'NONE', #3658, .T. ) ;
#8819=CIRCLE ( 'NONE', #6057, 0.003937007874015749712 ) ;
#8855=VERTEX_POINT ( 'NONE', #14787 ) ;
#8887=DIRECTION ( 'NONE',  ( 0.000000000000000000, 0.000000000000000000, 1.000000000000000000 ) ) ;
#8929=VECTOR ( 'NONE', #13816, 39.37007874015748143 ) ;
#8939=EDGE_CURVE ( 'NONE', #11243, #5281, #8165, .T. ) ;
#8947=AXIS2_PLACEMENT_3D ( 'NONE', #10285, #4315, #9113 ) ;
#8973=DIRECTION ( 'NONE',  ( 0.000000000000000000, 0.000000000000000000, 1.000000000000000000 ) ) ;
#8980=CIRCLE ( 'NONE', #5455, 0.04330708661417324162 ) ;
#8996=ORIENTED_EDGE ( 'NONE', *, *, #8660, .T. ) ;
#9001=LINE ( 'NONE', #13774, #5312 ) ;
#9026=DIRECTION ( 'NONE',  ( -1.000000000000000000, 1.224646799147361096E-16, 0.000000000000000000 ) ) ;
#9040=VERTEX_POINT ( 'NONE', #8517 ) ;
#9046=DIRECTION ( 'NONE',  ( -1.000000000000000000, 0.000000000000000000, 0.000000000000000000 ) ) ;
#9048=ORIENTED_EDGE ( 'NONE', *, *, #352, .F. ) ;
#9113=DIRECTION ( 'NONE',  ( 1.000000000000000000, 0.000000000000000000, 0.000000000000000000 ) ) ;
#9114=CIRCLE ( 'NONE', #12128, 0.003937007874015749712 ) ;
#9123=ORIENTED_EDGE ( 'NONE', *, *, #9231, .F. ) ;
#9134=LINE ( 'NONE', #4427, #6848 ) ;
#9171=CIRCLE ( 'NONE', #8666, 0.003937007874015724558 ) ;
#9207=APPLICATION_CONTEXT ( 'automotive_design' ) ;
#9211=ADVANCED_FACE ( 'NONE', ( #13048 ), #7085, .T. ) ;
#9231=EDGE_CURVE ( 'NONE', #12221, #10241, #9171, .T. ) ;
#9239=ORIENTED_EDGE ( 'NONE', *, *, #15058, .T. ) ;
#9267=FACE_OUTER_BOUND ( 'NONE', #543, .T. ) ;
#9302=DIRECTION ( 'NONE',  ( 0.000000000000000000, 0.000000000000000000, 1.000000000000000000 ) ) ;
#9304=DIRECTION ( 'NONE',  ( 0.000000000000000000, 0.000000000000000000, 1.000000000000000000 ) ) ;
#9402=AXIS2_PLACEMENT_3D ( 'NONE', #14800, #12456, #11192 ) ;
#9408=CIRCLE ( 'NONE', #8149, 0.003937007874015749712 ) ;
#9422=DIRECTION ( 'NONE',  ( 0.000000000000000000, 0.000000000000000000, 1.000000000000000000 ) ) ;
#9423=AXIS2_PLACEMENT_3D ( 'NONE', #1516, #13495, #13561 ) ;
#9433=DIRECTION ( 'NONE',  ( -1.000000000000000000, 0.000000000000000000, 0.000000000000000000 ) ) ;
#9434=ADVANCED_FACE ( 'NONE', ( #14838 ), #7713, .T. ) ;
#9451=EDGE_LOOP ( 'NONE', ( #13000, #2965, #14591, #2342 ) ) ;
#9459=TOROIDAL_SURFACE ( 'NONE', #8947, 0.1240157480314959815, 0.003937007874015747977 ) ;
#9464=EDGE_CURVE ( 'NONE', #9877, #13444, #6591, .T. ) ;
#9470=ORIENTED_EDGE ( 'NONE', *, *, #10361, .F. ) ;
#9481=EDGE_CURVE ( 'NONE', #11443, #6019, #11545, .T. ) ;
#9499=CARTESIAN_POINT ( 'NONE',  ( -1.181102362204724310, -0.1240157480314959815, 0.02559055118110236185 ) ) ;
#9503=EDGE_CURVE ( 'NONE', #4974, #5718, #4665, .T. ) ;
#9509=CARTESIAN_POINT ( 'NONE',  ( 1.137795275590550936, 4.097147066950659020E-16, 0.02952755905511811330 ) ) ;
#9526=LINE ( 'NONE', #8497, #14364 ) ;
#9541=VERTEX_POINT ( 'NONE', #2058 ) ;
#9549=ORIENTED_EDGE ( 'NONE', *, *, #13446, .T. ) ;
#9573=DIRECTION ( 'NONE',  ( -1.000000000000000000, 0.000000000000000000, 0.000000000000000000 ) ) ;
#9574=EDGE_LOOP ( 'NONE', ( #6928, #14107, #11826, #9835 ) ) ;
#9587=TOROIDAL_SURFACE ( 'NONE', #14078, 0.04330708661417329020, 0.003937007874015747977 ) ;
#9602=CIRCLE ( 'NONE', #6578, 0.003937007874015749712 ) ;
#9608=EDGE_LOOP ( 'NONE', ( #2770, #13295, #3435, #14059 ) ) ;
#9665=DIRECTION ( 'NONE',  ( 0.000000000000000000, 0.000000000000000000, 1.000000000000000000 ) ) ;
#9690=CIRCLE ( 'NONE', #12444, 0.003937007874015749712 ) ;
#9703=VECTOR ( 'NONE', #7411, 39.37007874015748143 ) ;
#9720=VERTEX_POINT ( 'NONE', #5319 ) ;
#9722=CARTESIAN_POINT ( 'NONE',  ( 1.181102362204724310, 4.044111181948214319E-16, 0.02559055118110236185 ) ) ;
#9743=DIRECTION ( 'NONE',  ( -0.000000000000000000, -0.000000000000000000, -1.000000000000000000 ) ) ;
#9769=DIRECTION ( 'NONE',  ( 1.224646799147353207E-16, 1.000000000000000000, -0.000000000000000000 ) ) ;
#9777=DIRECTION ( 'NONE',  ( 1.000000000000000000, 0.000000000000000000, -0.000000000000000000 ) ) ;
#9789=EDGE_CURVE ( 'NONE', #9720, #4762, #6657, .T. ) ;
#9791=DIRECTION ( 'NONE',  ( 1.000000000000000000, 0.000000000000000000, 0.000000000000000000 ) ) ;
#9835=ORIENTED_EDGE ( 'NONE', *, *, #8555, .T. ) ;
#9842=DIRECTION ( 'NONE',  ( 1.000000000000000000, 0.000000000000000000, 0.000000000000000000 ) ) ;
#9843=CARTESIAN_POINT ( 'NONE',  ( -1.181102362204724310, 0.000000000000000000, 0.02559055118110236185 ) ) ;
#9855=EDGE_LOOP ( 'NONE', ( #13312, #14288, #1181, #7964 ) ) ;
#9867=CARTESIAN_POINT ( 'NONE',  ( -1.141732283464566677, 4.821444091131319228E-18, 0.02952755905511811330 ) ) ;
#9876=DIRECTION ( 'NONE',  ( 1.000000000000000000, 0.000000000000000000, 0.000000000000000000 ) ) ;
#9877=VERTEX_POINT ( 'NONE', #15368 ) ;
#9898=EDGE_CURVE ( 'NONE', #12256, #1879, #11185, .T. ) ;
#9902=CIRCLE ( 'NONE', #4373, 0.03937007874015751446 ) ;
#9946=EDGE_LOOP ( 'NONE', ( #7334, #6314, #14754, #4635 ) ) ;
#9986=DIRECTION ( 'NONE',  ( -1.000000000000000000, 0.000000000000000000, 0.000000000000000000 ) ) ;
#9993=DIRECTION ( 'NONE',  ( 0.000000000000000000, 0.000000000000000000, 1.000000000000000000 ) ) ;
#9997=EDGE_CURVE ( 'NONE', #8022, #10241, #13945, .T. ) ;
#9999=( LENGTH_UNIT ( ) NAMED_UNIT ( * ) SI_UNIT ( $, .METRE. ) );
#10051=CARTESIAN_POINT ( 'NONE',  ( -1.181102362204724310, 0.1240157480314959815, -0.02952755905511811330 ) ) ;
#10052=CARTESIAN_POINT ( 'NONE',  ( -1.220472440944881720, 0.000000000000000000, -0.02559055118110236185 ) ) ;
#10075=EDGE_CURVE ( 'NONE', #14099, #12256, #4187, .T. ) ;
#10076=TOROIDAL_SURFACE ( 'NONE', #3324, 0.04330708661417329020, 0.003937007874015747977 ) ;
#10080=ORIENTED_EDGE ( 'NONE', *, *, #9464, .F. ) ;
#10083=ADVANCED_FACE ( 'NONE', ( #5689 ), #3512, .F. ) ;
#10100=AXIS2_PLACEMENT_3D ( 'NONE', #4360, #3266, #8037 ) ;
#10104=AXIS2_PLACEMENT_3D ( 'NONE', #12497, #7474, #1525 ) ;
#10119=ADVANCED_FACE ( 'NONE', ( #14544 ), #2718, .F. ) ;
#10122=AXIS2_PLACEMENT_3D ( 'NONE', #2764, #7534, #10831 ) ;
#10139=EDGE_CURVE ( 'NONE', #624, #4871, #12275, .T. ) ;
#10144=CARTESIAN_POINT ( 'NONE',  ( 1.181102362204724310, 4.044111181948214319E-16, 0.02952755905511811330 ) ) ;
#10232=ADVANCED_FACE ( 'NONE', ( #2547 ), #1206, .T. ) ;
#10241=VERTEX_POINT ( 'NONE', #5042 ) ;
#10251=CARTESIAN_POINT ( 'NONE',  ( -1.181102362204724310, 0.000000000000000000, 0.02559055118110236185 ) ) ;
#10259=ORIENTED_EDGE ( 'NONE', *, *, #5600, .T. ) ;
#10260=EDGE_CURVE ( 'NONE', #4871, #15235, #12220, .T. ) ;
#10285=CARTESIAN_POINT ( 'NONE',  ( 1.181102362204724310, 4.044111181948214319E-16, -0.02559055118110236185 ) ) ;
#10337=CIRCLE ( 'NONE', #12111, 0.03937007874015751446 ) ;
#10361=EDGE_CURVE ( 'NONE', #9040, #14723, #8980, .T. ) ;
#10362=VERTEX_POINT ( 'NONE', #1769 ) ;
#10459=EDGE_LOOP ( 'NONE', ( #6705, #3480, #8452, #4546, #7573 ) ) ;
#10471=CIRCLE ( 'NONE', #4949, 0.1279527559055117780 ) ;
#10485=DIRECTION ( 'NONE',  ( 0.000000000000000000, 0.000000000000000000, -1.000000000000000000 ) ) ;
#10487=CARTESIAN_POINT ( 'NONE',  ( -1.141732283464566677, 4.821444091131322309E-18, -0.02559055118110236185 ) ) ;
#10499=LINE ( 'NONE', #14653, #7932 ) ;
#10545=EDGE_CURVE ( 'NONE', #11243, #9720, #2447, .T. ) ;
#10579=DIRECTION ( 'NONE',  ( 1.000000000000000000, 0.000000000000000000, 0.000000000000000000 ) ) ;
#10603=VERTEX_POINT ( 'NONE', #7590 ) ;
#10690=CIRCLE ( 'NONE', #12430, 0.04330708661417324162 ) ;
#10711=ORIENTED_EDGE ( 'NONE', *, *, #10075, .T. ) ;
#10716=CARTESIAN_POINT ( 'NONE',  ( 1.137795275590550936, 4.097147066950659020E-16, -0.02559055118110236185 ) ) ;
#10804=CARTESIAN_POINT ( 'NONE',  ( -1.181102362204724310, 0.1240157480314959815, -0.02952755905511811330 ) ) ;
#10813=EDGE_CURVE ( 'NONE', #12795, #5281, #5945, .T. ) ;
#10831=DIRECTION ( 'NONE',  ( 1.000000000000000000, 0.000000000000000000, 0.000000000000000000 ) ) ;
#10883=DIRECTION ( 'NONE',  ( 1.000000000000000000, -0.000000000000000000, 0.000000000000000000 ) ) ;
#10923=CYLINDRICAL_SURFACE ( 'NONE', #11893, 0.003937007874015749712 ) ;
#10953=EDGE_CURVE ( 'NONE', #9541, #4974, #10499, .T. ) ;
#10954=ORIENTED_EDGE ( 'NONE', *, *, #6988, .F. ) ;
#10961=LINE ( 'NONE', #9867, #1635 ) ;
#10969=( GEOMETRIC_REPRESENTATION_CONTEXT ( 3 ) GLOBAL_UNCERTAINTY_ASSIGNED_CONTEXT ( ( #11276 ) ) GLOBAL_UNIT_ASSIGNED_CONTEXT ( ( #11246, #521, #11167 ) ) REPRESENTATION_CONTEXT ( 'NONE', 'WORKASPACE' ) );
#10987=CARTESIAN_POINT ( 'NONE',  ( -1.181102362204724310, 0.000000000000000000, -0.02559055118110236185 ) ) ;
#11001=CARTESIAN_POINT ( 'NONE',  ( -1.181102362204724310, 0.1279527559055117225, -0.02559055118110236185 ) ) ;
#11013=CARTESIAN_POINT ( 'NONE',  ( -1.181102362204724310, 0.1240157480314959815, -0.02559055118110236185 ) ) ;
#11048=DIRECTION ( 'NONE',  ( 1.000000000000000000, 0.000000000000000000, 0.000000000000000000 ) ) ;
#11075=SHAPE_REPRESENTATION ( 'Connecting Link', ( #11481 ), #10969 ) ;
#11089=ORIENTED_EDGE ( 'NONE', *, *, #14286, .F. ) ;
#11100=DIRECTION ( 'NONE',  ( -1.000000000000000000, 0.000000000000000000, 0.000000000000000000 ) ) ;
#11123=EDGE_CURVE ( 'NONE', #2263, #12795, #1688, .T. ) ;
#11136=CIRCLE ( 'NONE', #11909, 0.1240157480314959260 ) ;
#11164=ADVANCED_BREP_SHAPE_REPRESENTATION ( '', ( #14611, #11481 ), #10969 ) ;
#11167=( NAMED_UNIT ( * ) SI_UNIT ( $, .STERADIAN. ) SOLID_ANGLE_UNIT ( ) );
#11172=DIRECTION ( 'NONE',  ( -0.000000000000000000, -0.000000000000000000, -1.000000000000000000 ) ) ;
#11185=CIRCLE ( 'NONE', #5164, 0.04330708661417324162 ) ;
#11192=DIRECTION ( 'NONE',  ( 1.000000000000000000, 0.000000000000000000, 0.000000000000000000 ) ) ;
#11201=AXIS2_PLACEMENT_3D ( 'NONE', #2070, #14814, #493 ) ;
#11243=VERTEX_POINT ( 'NONE', #10487 ) ;
#11246=( CONVERSION_BASED_UNIT ( 'INCH', #6460 ) LENGTH_UNIT ( ) NAMED_UNIT ( #15269 ) );
#11247=DIRECTION ( 'NONE',  ( 1.000000000000000000, 0.000000000000000000, 0.000000000000000000 ) ) ;
#11268=CARTESIAN_POINT ( 'NONE',  ( -1.141732283464566677, 4.821444091131322309E-18, 0.02559055118110236185 ) ) ;
#11276=UNCERTAINTY_MEASURE_WITH_UNIT (LENGTH_MEASURE( 1.000000000000000082E-05 ), #11246, 'distance_accuracy_value', 'NONE');
#11296=DIRECTION ( 'NONE',  ( 0.000000000000000000, 0.000000000000000000, -1.000000000000000000 ) ) ;
#11307=EDGE_CURVE ( 'NONE', #12795, #2263, #12084, .T. ) ;
#11347=EDGE_CURVE ( 'NONE', #13444, #15235, #8819, .T. ) ;
#11368=EDGE_CURVE ( 'NONE', #12169, #14199, #2640, .T. ) ;
#11381=AXIS2_PLACEMENT_3D ( 'NONE', #13485, #8626, #2749 ) ;
#11387=ORIENTED_EDGE ( 'NONE', *, *, #6178, .T. ) ;
#11406=CARTESIAN_POINT ( 'NONE',  ( -1.181102362204724310, 0.000000000000000000, -0.02952755905511811330 ) ) ;
#11408=DIRECTION ( 'NONE',  ( 0.000000000000000000, 0.000000000000000000, 1.000000000000000000 ) ) ;
#11410=ADVANCED_FACE ( 'NONE', ( #294 ), #9587, .T. ) ;
#11425=CARTESIAN_POINT ( 'NONE',  ( 1.181102362204724310, 4.044111181948214319E-16, 0.02559055118110236185 ) ) ;
#11443=VERTEX_POINT ( 'NONE', #12343 ) ;
#11451=CARTESIAN_POINT ( 'NONE',  ( 1.305118110236220152, 4.044111181948214319E-16, 0.02952755905511811330 ) ) ;
#11480=CARTESIAN_POINT ( 'NONE',  ( -1.181102362204724310, -0.1279527559055117225, 0.02559055118110236185 ) ) ;
#11481=AXIS2_PLACEMENT_3D ( 'NONE', #12576, #4264, #5441 ) ;
#11486=ADVANCED_FACE ( 'NONE', ( #13518 ), #8329, .T. ) ;
#11496=ORIENTED_EDGE ( 'NONE', *, *, #3979, .T. ) ;
#11538=CARTESIAN_POINT ( 'NONE',  ( 1.181102362204724310, 4.044111181948214319E-16, -0.02559055118110236185 ) ) ;
#11545=LINE ( 'NONE', #11480, #8929 ) ;
#11557=EDGE_CURVE ( 'NONE', #10362, #12169, #3088, .T. ) ;
#11579=ORIENTED_EDGE ( 'NONE', *, *, #8562, .F. ) ;
#11583=AXIS2_PLACEMENT_3D ( 'NONE', #1620, #6380, #66 ) ;
#11619=VERTEX_POINT ( 'NONE', #13286 ) ;
#11646=CARTESIAN_POINT ( 'NONE',  ( 1.181102362204724310, 0.1240157480314963978, -0.02559055118110236185 ) ) ;
#11728=DIRECTION ( 'NONE',  ( -0.000000000000000000, -0.000000000000000000, -1.000000000000000000 ) ) ;
#11736=CARTESIAN_POINT ( 'NONE',  ( 1.181102362204724310, 4.044111181948214319E-16, 0.02952755905511811330 ) ) ;
#11743=ORIENTED_EDGE ( 'NONE', *, *, #7014, .T. ) ;
#11752=DIRECTION ( 'NONE',  ( 0.000000000000000000, 0.000000000000000000, 1.000000000000000000 ) ) ;
#11757=CARTESIAN_POINT ( 'NONE',  ( 1.220472440944881720, 4.092325622859527280E-16, 0.02952755905511811330 ) ) ;
#11761=EDGE_LOOP ( 'NONE', ( #1583, #12178 ) ) ;
#11826=ORIENTED_EDGE ( 'NONE', *, *, #2311, .T. ) ;
#11843=VECTOR ( 'NONE', #6939, 39.37007874015748143 ) ;
#11846=ADVANCED_FACE ( 'NONE', ( #15245 ), #14146, .T. ) ;
#11855=CARTESIAN_POINT ( 'NONE',  ( 1.305118110236220152, 4.044111181948214319E-16, -0.02559055118110236185 ) ) ;
#11881=DIRECTION ( 'NONE',  ( -1.000000000000000000, 0.000000000000000000, 0.000000000000000000 ) ) ;
#11893=AXIS2_PLACEMENT_3D ( 'NONE', #14532, #4520, #9302 ) ;
#11905=( LENGTH_UNIT ( ) NAMED_UNIT ( * ) SI_UNIT ( $, .METRE. ) );
#11909=AXIS2_PLACEMENT_3D ( 'NONE', #4458, #1573, #5170 ) ;
#11930=DIRECTION ( 'NONE',  ( 0.000000000000000000, 0.000000000000000000, 1.000000000000000000 ) ) ;
#12010=EDGE_CURVE ( 'NONE', #12092, #8855, #9114, .T. ) ;
#12012=EDGE_CURVE ( 'NONE', #1879, #12256, #12362, .T. ) ;
#12043=ORIENTED_EDGE ( 'NONE', *, *, #10545, .T. ) ;
#12084=CIRCLE ( 'NONE', #2077, 0.03937007874015751446 ) ;
#12086=ADVANCED_FACE ( 'NONE', ( #6507 ), #803, .T. ) ;
#12092=VERTEX_POINT ( 'NONE', #7849 ) ;
#12104=DIRECTION ( 'NONE',  ( 1.000000000000000000, 0.000000000000000000, 0.000000000000000000 ) ) ;
#12111=AXIS2_PLACEMENT_3D ( 'NONE', #14847, #6602, #456 ) ;
#12128=AXIS2_PLACEMENT_3D ( 'NONE', #3951, #9986, #8729 ) ;
#12146=FACE_OUTER_BOUND ( 'NONE', #357, .T. ) ;
#12169=VERTEX_POINT ( 'NONE', #1988 ) ;
#12178=ORIENTED_EDGE ( 'NONE', *, *, #2264, .T. ) ;
#12197=AXIS2_PLACEMENT_3D ( 'NONE', #876, #9422, #13964 ) ;
#12220=CIRCLE ( 'NONE', #6683, 0.1240157480314959260 ) ;
#12221=VERTEX_POINT ( 'NONE', #9509 ) ;
#12229=CARTESIAN_POINT ( 'NONE',  ( 1.181102362204724310, 4.044111181948214319E-16, -0.02559055118110236185 ) ) ;
#12243=ORIENTED_EDGE ( 'NONE', *, *, #6244, .F. ) ;
#12245=DIRECTION ( 'NONE',  ( 0.000000000000000000, 0.000000000000000000, 1.000000000000000000 ) ) ;
#12249=ORIENTED_EDGE ( 'NONE', *, *, #10260, .F. ) ;
#12256=VERTEX_POINT ( 'NONE', #6993 ) ;
#12275=LINE ( 'NONE', #3741, #9703 ) ;
#12284=ORIENTED_EDGE ( 'NONE', *, *, #2311, .F. ) ;
#12300=ADVANCED_FACE ( 'NONE', ( #3398, #4485, #9267 ), #14576, .T. ) ;
#12343=CARTESIAN_POINT ( 'NONE',  ( 1.181102362204724310, -0.1279527559055113062, 0.02559055118110236185 ) ) ;
#12362=CIRCLE ( 'NONE', #10122, 0.04330708661417324162 ) ;
#12364=EDGE_CURVE ( 'NONE', #14723, #9040, #12640, .T. ) ;
#12372=DIRECTION ( 'NONE',  ( 1.224646799147353207E-16, 1.000000000000000000, -0.000000000000000000 ) ) ;
#12403=VECTOR ( 'NONE', #9433, 39.37007874015748143 ) ;
#12404=ORIENTED_EDGE ( 'NONE', *, *, #11347, .F. ) ;
#12405=ORIENTED_EDGE ( 'NONE', *, *, #7518, .T. ) ;
#12412=TOROIDAL_SURFACE ( 'NONE', #7651, 0.04330708661417329020, 0.003937007874015747977 ) ;
#12430=AXIS2_PLACEMENT_3D ( 'NONE', #869, #4625, #3144 ) ;
#12444=AXIS2_PLACEMENT_3D ( 'NONE', #15227, #5333, #8973 ) ;
#12449=AXIS2_PLACEMENT_3D ( 'NONE', #8281, #13056, #14312 ) ;
#12456=DIRECTION ( 'NONE',  ( 0.000000000000000000, 0.000000000000000000, 1.000000000000000000 ) ) ;
#12477=ORIENTED_EDGE ( 'NONE', *, *, #8562, .T. ) ;
#12494=FACE_OUTER_BOUND ( 'NONE', #4169, .T. ) ;
#12497=CARTESIAN_POINT ( 'NONE',  ( -1.181102362204724310, -0.1240157480314959815, -0.02559055118110236185 ) ) ;
#12500=DIRECTION ( 'NONE',  ( -0.000000000000000000, -0.000000000000000000, -1.000000000000000000 ) ) ;
#12539=UNCERTAINTY_MEASURE_WITH_UNIT (LENGTH_MEASURE( 1.000000000000000082E-05 ), #2257, 'distance_accuracy_value', 'NONE');
#12548=DIRECTION ( 'NONE',  ( 0.000000000000000000, 0.000000000000000000, 1.000000000000000000 ) ) ;
#12576=CARTESIAN_POINT ( 'NONE',  ( 0.000000000000000000, 0.000000000000000000, 0.000000000000000000 ) ) ;
#12632=ORIENTED_EDGE ( 'NONE', *, *, #9231, .T. ) ;
#12640=CIRCLE ( 'NONE', #11381, 0.04330708661417324162 ) ;
#12697=ADVANCED_FACE ( 'NONE', ( #8606 ), #1158, .T. ) ;
#12698=PRODUCT_DEFINITION_CONTEXT ( 'detailed design', #9207, 'design' ) ;
#12734=EDGE_CURVE ( 'NONE', #11619, #4513, #6121, .T. ) ;
#12742=EDGE_LOOP ( 'NONE', ( #14033, #6790, #7732, #7140 ) ) ;
#12765=ORIENTED_EDGE ( 'NONE', *, *, #2264, .F. ) ;
#12774=EDGE_CURVE ( 'NONE', #2263, #11243, #10961, .T. ) ;
#12789=CARTESIAN_POINT ( 'NONE',  ( -1.181102362204724310, 0.1240157480314959815, 0.02952755905511811330 ) ) ;
#12795=VERTEX_POINT ( 'NONE', #7666 ) ;
#12832=ADVANCED_FACE ( 'NONE', ( #7567 ), #1892, .T. ) ;
#12833=ORIENTED_EDGE ( 'NONE', *, *, #7926, .T. ) ;
#12887=EDGE_CURVE ( 'NONE', #6733, #1879, #2637, .T. ) ;
#12897=CARTESIAN_POINT ( 'NONE',  ( 1.181102362204724310, 4.044111181948214319E-16, -0.02559055118110236185 ) ) ;
#12898=CARTESIAN_POINT ( 'NONE',  ( 1.305118110236220152, 4.044111181948214319E-16, -0.02952755905511811330 ) ) ;
#12912=FACE_OUTER_BOUND ( 'NONE', #14525, .T. ) ;
#12942=CIRCLE ( 'NONE', #2185, 0.003937007874015724558 ) ;
#12963=ORIENTED_EDGE ( 'NONE', *, *, #522, .T. ) ;
#12976=VECTOR ( 'NONE', #2114, 39.37007874015748143 ) ;
#12978=DIRECTION ( 'NONE',  ( 0.000000000000000000, 0.000000000000000000, 1.000000000000000000 ) ) ;
#12986=EDGE_CURVE ( 'NONE', #14723, #2263, #6366, .T. ) ;
#13000=ORIENTED_EDGE ( 'NONE', *, *, #15154, .F. ) ;
#13030=CARTESIAN_POINT ( 'NONE',  ( -1.137795275590550936, 0.000000000000000000, 0.02952755905511811330 ) ) ;
#13048=FACE_OUTER_BOUND ( 'NONE', #9946, .T. ) ;
#13056=DIRECTION ( 'NONE',  ( -0.000000000000000000, -0.000000000000000000, -1.000000000000000000 ) ) ;
#13060=CARTESIAN_POINT ( 'NONE',  ( -1.181102362204724310, -0.1279527559055117225, 0.02559055118110236185 ) ) ;
#13066=ORIENTED_EDGE ( 'NONE', *, *, #15154, .T. ) ;
#13082=ADVANCED_FACE ( 'NONE', ( #2639 ), #7412, .T. ) ;
#13113=DIRECTION ( 'NONE',  ( 1.000000000000000000, 0.000000000000000000, 0.000000000000000000 ) ) ;
#13123=CIRCLE ( 'NONE', #1358, 0.1279527559055117780 ) ;
#13137=CIRCLE ( 'NONE', #7378, 0.03937007874015751446 ) ;
#13176=VECTOR ( 'NONE', #5338, 39.37007874015748143 ) ;
#13202=ORIENTED_EDGE ( 'NONE', *, *, #12734, .F. ) ;
#13217=ORIENTED_EDGE ( 'NONE', *, *, #9464, .T. ) ;
#13286=CARTESIAN_POINT ( 'NONE',  ( -1.309055118110236116, 0.000000000000000000, 0.02559055118110236185 ) ) ;
#13293=DIRECTION ( 'NONE',  ( -0.000000000000000000, -0.000000000000000000, -1.000000000000000000 ) ) ;
#13295=ORIENTED_EDGE ( 'NONE', *, *, #11368, .F. ) ;
#13312=ORIENTED_EDGE ( 'NONE', *, *, #1680, .F. ) ;
#13330=EDGE_CURVE ( 'NONE', #14199, #2506, #7906, .T. ) ;
#13348=CARTESIAN_POINT ( 'NONE',  ( 1.181102362204724310, 0.1279527559055117225, 0.02952755905511811330 ) ) ;
#13352=DIRECTION ( 'NONE',  ( -1.000000000000000000, 1.224646799147296261E-16, 0.000000000000000000 ) ) ;
#13360=ADVANCED_FACE ( 'NONE', ( #2536 ), #13913, .T. ) ;
#13362=CARTESIAN_POINT ( 'NONE',  ( -1.181102362204724310, 0.000000000000000000, 0.02559055118110236185 ) ) ;
#13370=DIRECTION ( 'NONE',  ( -1.000000000000000000, 0.000000000000000000, 0.000000000000000000 ) ) ;
#13381=CLOSED_SHELL ( 'NONE', ( #13360, #2944, #10232, #3676, #12832, #12697, #10083, #5573, #11846, #12300, #7987, #12086, #10119, #9434, #1272, #4773, #6435, #11410, #4714, #6047, #13933, #1755, #5173, #2507, #8003, #11486, #13082, #9211, #526 ) ) ;
#13399=AXIS2_PLACEMENT_3D ( 'NONE', #5060, #2658, #1490 ) ;
#13444=VERTEX_POINT ( 'NONE', #11001 ) ;
#13446=EDGE_CURVE ( 'NONE', #8855, #9877, #4806, .T. ) ;
#13485=CARTESIAN_POINT ( 'NONE',  ( -1.181102362204724310, 0.000000000000000000, 0.02952755905511811330 ) ) ;
#13495=DIRECTION ( 'NONE',  ( -0.000000000000000000, -0.000000000000000000, -1.000000000000000000 ) ) ;
#13518=FACE_OUTER_BOUND ( 'NONE', #9855, .T. ) ;
#13561=DIRECTION ( 'NONE',  ( -1.000000000000000000, 0.000000000000000000, 0.000000000000000000 ) ) ;
#13566=LINE ( 'NONE', #10051, #6580 ) ;
#13570=CARTESIAN_POINT ( 'NONE',  ( 1.309055118110236116, 4.044111181948214319E-16, -0.02559055118110236185 ) ) ;
#13689=CARTESIAN_POINT ( 'NONE',  ( 1.224409448818897461, 4.044111181948214319E-16, 0.02559055118110236185 ) ) ;
#13774=CARTESIAN_POINT ( 'NONE',  ( 1.181102362204724310, -0.1279527559055113062, 0.02952755905511811330 ) ) ;
#13812=ORIENTED_EDGE ( 'NONE', *, *, #14286, .T. ) ;
#13816=DIRECTION ( 'NONE',  ( -1.000000000000000000, 0.000000000000000000, -0.000000000000000000 ) ) ;
#13824=DIRECTION ( 'NONE',  ( -0.000000000000000000, -0.000000000000000000, -1.000000000000000000 ) ) ;
#13860=TOROIDAL_SURFACE ( 'NONE', #14617, 0.1240157480314959815, 0.003937007874015747977 ) ;
#13913=TOROIDAL_SURFACE ( 'NONE', #14166, 0.1240157480314959815, 0.003937007874015747977 ) ;
#13914=PRODUCT_DEFINITION_SHAPE ( 'NONE', 'NONE',  #15321 ) ;
#13933=ADVANCED_FACE ( 'NONE', ( #8784 ), #4684, .T. ) ;
#13945=CIRCLE ( 'NONE', #7187, 0.03937007874015751446 ) ;
#13959=DIRECTION ( 'NONE',  ( -1.000000000000000000, 0.000000000000000000, 0.000000000000000000 ) ) ;
#13964=DIRECTION ( 'NONE',  ( 1.000000000000000000, 0.000000000000000000, 0.000000000000000000 ) ) ;
#13973=DIRECTION ( 'NONE',  ( -1.000000000000000000, 0.000000000000000000, 0.000000000000000000 ) ) ;
#14019=EDGE_CURVE ( 'NONE', #624, #14199, #5411, .T. ) ;
#14033=ORIENTED_EDGE ( 'NONE', *, *, #11307, .T. ) ;
#14059=ORIENTED_EDGE ( 'NONE', *, *, #10139, .F. ) ;
#14061=DIRECTION ( 'NONE',  ( -0.000000000000000000, -0.000000000000000000, -1.000000000000000000 ) ) ;
#14078=AXIS2_PLACEMENT_3D ( 'NONE', #4980, #7261, #7413 ) ;
#14099=VERTEX_POINT ( 'NONE', #5545 ) ;
#14102=DIRECTION ( 'NONE',  ( 1.000000000000000000, 0.000000000000000000, 0.000000000000000000 ) ) ;
#14105=DIRECTION ( 'NONE',  ( 0.000000000000000000, 0.000000000000000000, 1.000000000000000000 ) ) ;
#14107=ORIENTED_EDGE ( 'NONE', *, *, #12734, .T. ) ;
#14108=CIRCLE ( 'NONE', #600, 0.1240157480314959260 ) ;
#14118=EDGE_CURVE ( 'NONE', #4762, #9720, #10690, .T. ) ;
#14146=CYLINDRICAL_SURFACE ( 'NONE', #1095, 0.1279527559055117780 ) ;
#14161=AXIS2_PLACEMENT_3D ( 'NONE', #13689, #14854, #1772 ) ;
#14166=AXIS2_PLACEMENT_3D ( 'NONE', #3652, #8426, #12104 ) ;
#14194=ORIENTED_EDGE ( 'NONE', *, *, #918, .F. ) ;
#14199=VERTEX_POINT ( 'NONE', #1420 ) ;
#14247=CARTESIAN_POINT ( 'NONE',  ( -1.137795275590550936, 0.000000000000000000, 0.02559055118110236185 ) ) ;
#14254=ORIENTED_EDGE ( 'NONE', *, *, #6840, .T. ) ;
#14286=EDGE_CURVE ( 'NONE', #5281, #4762, #12942, .T. ) ;
#14288=ORIENTED_EDGE ( 'NONE', *, *, #7777, .F. ) ;
#14312=DIRECTION ( 'NONE',  ( -1.000000000000000000, 0.000000000000000000, 0.000000000000000000 ) ) ;
#14364=VECTOR ( 'NONE', #2611, 39.37007874015748143 ) ;
#14377=DIRECTION ( 'NONE',  ( 1.000000000000000000, 0.000000000000000000, 0.000000000000000000 ) ) ;
#14378=CARTESIAN_POINT ( 'NONE',  ( -1.181102362204724310, 0.000000000000000000, -0.02952755905511811330 ) ) ;
#14439=AXIS2_PLACEMENT_3D ( 'NONE', #11538, #8887, #741 ) ;
#14481=DIRECTION ( 'NONE',  ( 0.000000000000000000, 0.000000000000000000, -1.000000000000000000 ) ) ;
#14493=DIRECTION ( 'NONE',  ( 0.000000000000000000, 0.000000000000000000, 1.000000000000000000 ) ) ;
#14494=DIRECTION ( 'NONE',  ( -0.000000000000000000, -0.000000000000000000, -1.000000000000000000 ) ) ;
#14501=ORIENTED_EDGE ( 'NONE', *, *, #11347, .T. ) ;
#14511=DIRECTION ( 'NONE',  ( 1.000000000000000000, 0.000000000000000000, 0.000000000000000000 ) ) ;
#14525=EDGE_LOOP ( 'NONE', ( #9549, #13217, #12284, #12405 ) ) ;
#14532=CARTESIAN_POINT ( 'NONE',  ( -1.181102362204724310, 0.1240157480314959815, -0.02559055118110236185 ) ) ;
#14544=FACE_OUTER_BOUND ( 'NONE', #2223, .T. ) ;
#14576=PLANE ( 'NONE',  #5091 ) ;
#14591=ORIENTED_EDGE ( 'NONE', *, *, #9503, .F. ) ;
#14611=MANIFOLD_SOLID_BREP ( 'Fillet1', #13381 ) ;
#14617=AXIS2_PLACEMENT_3D ( 'NONE', #88, #11930, #14102 ) ;
#14624=AXIS2_PLACEMENT_3D ( 'NONE', #7566, #14494, #11100 ) ;
#14639=ORIENTED_EDGE ( 'NONE', *, *, #13330, .T. ) ;
#14640=ORIENTED_EDGE ( 'NONE', *, *, #14118, .F. ) ;
#14653=CARTESIAN_POINT ( 'NONE',  ( 1.181102362204724310, -0.1240157480314959815, 0.02952755905511811330 ) ) ;
#14668=VECTOR ( 'NONE', #50, 39.37007874015748143 ) ;
#14701=ORIENTED_EDGE ( 'NONE', *, *, #9789, .T. ) ;
#14703=ORIENTED_EDGE ( 'NONE', *, *, #11123, .T. ) ;
#14723=VERTEX_POINT ( 'NONE', #13030 ) ;
#14754=ORIENTED_EDGE ( 'NONE', *, *, #15058, .F. ) ;
#14756=DIRECTION ( 'NONE',  ( 1.000000000000000000, 0.000000000000000000, 0.000000000000000000 ) ) ;
#14783=CARTESIAN_POINT ( 'NONE',  ( -1.181102362204724310, 0.000000000000000000, -0.02559055118110236185 ) ) ;
#14787=CARTESIAN_POINT ( 'NONE',  ( 1.181102362204724310, 0.1279527559055117225, 0.02559055118110236185 ) ) ;
#14800=CARTESIAN_POINT ( 'NONE',  ( 1.181102362204724310, 4.044111181948214319E-16, 0.02559055118110236185 ) ) ;
#14814=DIRECTION ( 'NONE',  ( 0.000000000000000000, -1.000000000000000000, 0.000000000000000000 ) ) ;
#14815=DIRECTION ( 'NONE',  ( 1.000000000000000000, 0.000000000000000000, 0.000000000000000000 ) ) ;
#14816=ORIENTED_EDGE ( 'NONE', *, *, #11368, .T. ) ;
#14833=VECTOR ( 'NONE', #7489, 39.37007874015748143 ) ;
#14838=FACE_OUTER_BOUND ( 'NONE', #3148, .T. ) ;
#14847=CARTESIAN_POINT ( 'NONE',  ( 1.181102362204724310, 4.044111181948214319E-16, -0.02559055118110236185 ) ) ;
#14853=CIRCLE ( 'NONE', #10100, 0.04330708661417324162 ) ;
#14854=DIRECTION ( 'NONE',  ( 0.000000000000000000, -1.000000000000000000, 0.000000000000000000 ) ) ;
#14898=CIRCLE ( 'NONE', #1385, 0.003937007874015749712 ) ;
#14900=AXIS2_PLACEMENT_3D ( 'NONE', #8105, #7008, #4212 ) ;
#14933=DIRECTION ( 'NONE',  ( 1.000000000000000000, 0.000000000000000000, 0.000000000000000000 ) ) ;
#14964=DIRECTION ( 'NONE',  ( 0.000000000000000000, -1.000000000000000000, 0.000000000000000000 ) ) ;
#14989=DIRECTION ( 'NONE',  ( 1.224646799147353207E-16, 1.000000000000000000, -0.000000000000000000 ) ) ;
#14992=EDGE_LOOP ( 'NONE', ( #11089, #1603, #12043, #14640 ) ) ;
#14993=ORIENTED_EDGE ( 'NONE', *, *, #14118, .T. ) ;
#15058=EDGE_CURVE ( 'NONE', #6019, #9541, #3462, .T. ) ;
#15120=AXIS2_PLACEMENT_3D ( 'NONE', #11646, #11881, #5852 ) ;
#15154=EDGE_CURVE ( 'NONE', #8643, #11443, #10471, .T. ) ;
#15164=DIRECTION ( 'NONE',  ( -0.000000000000000000, -0.000000000000000000, -1.000000000000000000 ) ) ;
#15173=FACE_OUTER_BOUND ( 'NONE', #287, .T. ) ;
#15187=CARTESIAN_POINT ( 'NONE',  ( 1.181102362204724310, -0.1240157480314955790, 0.02952755905511811330 ) ) ;
#15213=( GEOMETRIC_REPRESENTATION_CONTEXT ( 3 ) GLOBAL_UNCERTAINTY_ASSIGNED_CONTEXT ( ( #12539 ) ) GLOBAL_UNIT_ASSIGNED_CONTEXT ( ( #2257, #6156, #1314 ) ) REPRESENTATION_CONTEXT ( 'NONE', 'WORKASPACE' ) );
#15227=CARTESIAN_POINT ( 'NONE',  ( 1.181102362204724310, -0.1240157480314955790, 0.02559055118110236185 ) ) ;
#15235=VERTEX_POINT ( 'NONE', #10804 ) ;
#15237=ORIENTED_EDGE ( 'NONE', *, *, #12012, .F. ) ;
#15245=FACE_OUTER_BOUND ( 'NONE', #6029, .T. ) ;
#15269=DIMENSIONAL_EXPONENTS ( 1.000000000000000000, 0.000000000000000000, 0.000000000000000000, 0.000000000000000000, 0.000000000000000000, 0.000000000000000000, 0.000000000000000000 ) ;
#15321=PRODUCT_DEFINITION ( 'UNKNOWN', '', #5106, #12698 ) ;
#15322=DIRECTION ( 'NONE',  ( -0.000000000000000000, -0.000000000000000000, -1.000000000000000000 ) ) ;
#15357=EDGE_CURVE ( 'NONE', #6019, #11619, #2717, .T. ) ;
#15368=CARTESIAN_POINT ( 'NONE',  ( 1.181102362204724310, 0.1279527559055117225, -0.02559055118110236185 ) ) ;
#15382=AXIS2_PLACEMENT_3D ( 'NONE', #6439, #7770, #13973 ) ;
#15417=AXIS2_PLACEMENT_3D ( 'NONE', #1479, #13293, #5048 ) ;
#15441=CARTESIAN_POINT ( 'NONE',  ( 1.181102362204724310, 4.044111181948214319E-16, 0.02559055118110236185 ) ) ;
#15513=COLOUR_RGB('Sky Blue',0.24,0.69,0.87);
#15514=FILL_AREA_STYLE_COLOUR('',#15513);
#15515=FILL_AREA_STYLE('',(#15514));
#15516=SURFACE_STYLE_FILL_AREA(#15515);
#15517=SURFACE_SIDE_STYLE('',(#15516));
#15518=SURFACE_STYLE_USAGE(.BOTH.,#15517);
#15519=PRESENTATION_STYLE_ASSIGNMENT((#15518));
ENDSEC;
END-ISO-10303-21;
